ISO-10303-21;
HEADER;
/* Generated by software containing ST-Developer
 * from STEP Tools, Inc. (www.steptools.com) 
 */

FILE_DESCRIPTION(
/* description */ ('Pipe clamp stand with threaded column'),
/* implementation_level */ '2;1');

FILE_NAME(
/* name */ 'Hex Nut - M8.step',
/* time_stamp */ '2026-10-27T10:55:48-07:00',
/* author */ (''),
/* organization */ (''),
/* preprocessor_version */ 'ST-DEVELOPER v20.2',
/* originating_system */ 'Autodesk Translation Framework v15.17.0.0',
/* authorisation */ '');

FILE_SCHEMA (('AUTOMOTIVE_DESIGN { 1 0 10303 214 3 1 1 }'));
ENDSEC;

DATA;
#10=MECHANICAL_DESIGN_GEOMETRIC_PRESENTATION_REPRESENTATION('',(#766),#34433);
#183=(
BOUNDED_CURVE()
B_SPLINE_CURVE(2,(#28836,#28837,#28838),.UNSPECIFIED.,.F.,.F.)
B_SPLINE_CURVE_WITH_KNOTS((3,3),(0.14973948338295,0.97160236658079),
 .UNSPECIFIED.)
CURVE()
GEOMETRIC_REPRESENTATION_ITEM()
RATIONAL_B_SPLINE_CURVE((1.07140024848292,1.23714644374248,1.07140024848292))
REPRESENTATION_ITEM('')
);
#184=(
BOUNDED_CURVE()
B_SPLINE_CURVE(2,(#28840,#28841,#28842),.UNSPECIFIED.,.F.,.F.)
B_SPLINE_CURVE_WITH_KNOTS((3,3),(0.14973948338295,0.971602366580789),
 .UNSPECIFIED.)
CURVE()
GEOMETRIC_REPRESENTATION_ITEM()
RATIONAL_B_SPLINE_CURVE((1.07140024848292,1.23714644374248,1.07140024848292))
REPRESENTATION_ITEM('')
);
#185=(
BOUNDED_CURVE()
B_SPLINE_CURVE(2,(#28847,#28848,#28849),.UNSPECIFIED.,.F.,.F.)
B_SPLINE_CURVE_WITH_KNOTS((3,3),(0.14973948338295,0.97160236658079),
 .UNSPECIFIED.)
CURVE()
GEOMETRIC_REPRESENTATION_ITEM()
RATIONAL_B_SPLINE_CURVE((1.07140024848292,1.23714644374248,1.07140024848292))
REPRESENTATION_ITEM('')
);
#186=(
BOUNDED_CURVE()
B_SPLINE_CURVE(2,(#28851,#28852,#28853),.UNSPECIFIED.,.F.,.F.)
B_SPLINE_CURVE_WITH_KNOTS((3,3),(0.14973948338295,0.97160236658079),
 .UNSPECIFIED.)
CURVE()
GEOMETRIC_REPRESENTATION_ITEM()
RATIONAL_B_SPLINE_CURVE((1.07140024848292,1.23714644374248,1.07140024848292))
REPRESENTATION_ITEM('')
);
#187=(
BOUNDED_CURVE()
B_SPLINE_CURVE(2,(#28855,#28856,#28857),.UNSPECIFIED.,.F.,.F.)
B_SPLINE_CURVE_WITH_KNOTS((3,3),(0.14973948338295,0.971602366580789),
 .UNSPECIFIED.)
CURVE()
GEOMETRIC_REPRESENTATION_ITEM()
RATIONAL_B_SPLINE_CURVE((1.07140024848292,1.23714644374248,1.07140024848292))
REPRESENTATION_ITEM('')
);
#188=(
BOUNDED_CURVE()
B_SPLINE_CURVE(2,(#28858,#28859,#28860),.UNSPECIFIED.,.F.,.F.)
B_SPLINE_CURVE_WITH_KNOTS((3,3),(0.14973948338295,0.97160236658079),
 .UNSPECIFIED.)
CURVE()
GEOMETRIC_REPRESENTATION_ITEM()
RATIONAL_B_SPLINE_CURVE((1.07140024848292,1.23714644374248,1.07140024848292))
REPRESENTATION_ITEM('')
);
#189=(
BOUNDED_CURVE()
B_SPLINE_CURVE(2,(#28867,#28868,#28869),.UNSPECIFIED.,.F.,.F.)
B_SPLINE_CURVE_WITH_KNOTS((3,3),(0.14973948338295,0.97160236658079),
 .UNSPECIFIED.)
CURVE()
GEOMETRIC_REPRESENTATION_ITEM()
RATIONAL_B_SPLINE_CURVE((1.07140024848292,1.23714644374248,1.07140024848292))
REPRESENTATION_ITEM('')
);
#190=(
BOUNDED_CURVE()
B_SPLINE_CURVE(2,(#28871,#28872,#28873),.UNSPECIFIED.,.F.,.F.)
B_SPLINE_CURVE_WITH_KNOTS((3,3),(0.14973948338295,0.97160236658079),
 .UNSPECIFIED.)
CURVE()
GEOMETRIC_REPRESENTATION_ITEM()
RATIONAL_B_SPLINE_CURVE((1.07140024848292,1.23714644374248,1.07140024848292))
REPRESENTATION_ITEM('')
);
#191=(
BOUNDED_CURVE()
B_SPLINE_CURVE(2,(#28875,#28876,#28877),.UNSPECIFIED.,.F.,.F.)
B_SPLINE_CURVE_WITH_KNOTS((3,3),(0.14973948338295,0.971602366580789),
 .UNSPECIFIED.)
CURVE()
GEOMETRIC_REPRESENTATION_ITEM()
RATIONAL_B_SPLINE_CURVE((1.07140024848292,1.23714644374248,1.07140024848292))
REPRESENTATION_ITEM('')
);
#192=(
BOUNDED_CURVE()
B_SPLINE_CURVE(2,(#28879,#28880,#28881),.UNSPECIFIED.,.F.,.F.)
B_SPLINE_CURVE_WITH_KNOTS((3,3),(0.14973948338295,0.97160236658079),
 .UNSPECIFIED.)
CURVE()
GEOMETRIC_REPRESENTATION_ITEM()
RATIONAL_B_SPLINE_CURVE((1.07140024848292,1.23714644374248,1.07140024848292))
REPRESENTATION_ITEM('')
);
#193=(
BOUNDED_CURVE()
B_SPLINE_CURVE(2,(#28883,#28884,#28885),.UNSPECIFIED.,.F.,.F.)
B_SPLINE_CURVE_WITH_KNOTS((3,3),(0.14973948338295,0.97160236658079),
 .UNSPECIFIED.)
CURVE()
GEOMETRIC_REPRESENTATION_ITEM()
RATIONAL_B_SPLINE_CURVE((1.07140024848292,1.23714644374248,1.07140024848292))
REPRESENTATION_ITEM('')
);
#194=(
BOUNDED_CURVE()
B_SPLINE_CURVE(2,(#28886,#28887,#28888),.UNSPECIFIED.,.F.,.F.)
B_SPLINE_CURVE_WITH_KNOTS((3,3),(0.14973948338295,0.971602366580789),
 .UNSPECIFIED.)
CURVE()
GEOMETRIC_REPRESENTATION_ITEM()
RATIONAL_B_SPLINE_CURVE((1.07140024848292,1.23714644374248,1.07140024848292))
REPRESENTATION_ITEM('')
);
#201=CONICAL_SURFACE('',#9571,0.734027674973257,1.0471975511966);
#202=CONICAL_SURFACE('',#9573,0.734027674973257,1.0471975511966);
#714=SHAPE_REPRESENTATION_RELATIONSHIP('SRR','None',#34556,#736);
#736=ADVANCED_BREP_SHAPE_REPRESENTATION('',(#794),#34424);
#766=STYLED_ITEM('',(#34750),#794);
#794=MANIFOLD_SOLID_BREP('Body1',#8795);
#847=FACE_BOUND('',#1985,.T.);
#848=FACE_BOUND('',#1987,.T.);
#1004=PLANE('',#9575);
#1005=PLANE('',#9576);
#1006=PLANE('',#9577);
#1007=PLANE('',#9581);
#1008=PLANE('',#9582);
#1009=PLANE('',#9583);
#1010=PLANE('',#9584);
#1011=PLANE('',#9585);
#1440=FACE_OUTER_BOUND('',#1975,.T.);
#1441=FACE_OUTER_BOUND('',#1976,.T.);
#1442=FACE_OUTER_BOUND('',#1977,.T.);
#1443=FACE_OUTER_BOUND('',#1978,.T.);
#1444=FACE_OUTER_BOUND('',#1979,.T.);
#1445=FACE_OUTER_BOUND('',#1980,.T.);
#1446=FACE_OUTER_BOUND('',#1981,.T.);
#1447=FACE_OUTER_BOUND('',#1982,.T.);
#1448=FACE_OUTER_BOUND('',#1983,.T.);
#1449=FACE_OUTER_BOUND('',#1984,.T.);
#1450=FACE_OUTER_BOUND('',#1986,.T.);
#1975=EDGE_LOOP('',(#7517,#7518,#7519,#7520,#7521,#7522,#7523,#7524,#7525));
#1976=EDGE_LOOP('',(#7526,#7527,#7528,#7529,#7530,#7531,#7532,#7533,#7534));
#1977=EDGE_LOOP('',(#7535,#7536,#7537,#7538));
#1978=EDGE_LOOP('',(#7539,#7540,#7541,#7542));
#1979=EDGE_LOOP('',(#7543,#7544,#7545,#7546));
#1980=EDGE_LOOP('',(#7547,#7548,#7549,#7550));
#1981=EDGE_LOOP('',(#7551,#7552,#7553,#7554));
#1982=EDGE_LOOP('',(#7555,#7556,#7557,#7558));
#1983=EDGE_LOOP('',(#7559,#7560,#7561,#7562));
#1984=EDGE_LOOP('',(#7563));
#1985=EDGE_LOOP('',(#7564));
#1986=EDGE_LOOP('',(#7565));
#1987=EDGE_LOOP('',(#7566));
#2580=LINE('',#28844,#3197);
#2581=LINE('',#28865,#3198);
#2582=LINE('',#28890,#3199);
#2583=LINE('',#28891,#3200);
#2584=LINE('',#28893,#3201);
#2585=LINE('',#28895,#3202);
#2586=LINE('',#28900,#3203);
#2587=LINE('',#28903,#3204);
#2588=LINE('',#28905,#3205);
#3197=VECTOR('',#11287,0.734027674973257);
#3198=VECTOR('',#11294,0.734027674973257);
#3199=VECTOR('',#11297,1.);
#3200=VECTOR('',#11298,1.);
#3201=VECTOR('',#11301,1.);
#3202=VECTOR('',#11304,1.);
#3203=VECTOR('',#11309,0.4);
#3204=VECTOR('',#11314,1.);
#3205=VECTOR('',#11317,1.);
#3424=CIRCLE('',#9572,0.6175);
#3425=CIRCLE('',#9574,0.6175);
#3426=CIRCLE('',#9579,0.338975);
#3427=CIRCLE('',#9580,0.338975);
#4110=VERTEX_POINT('',#28834);
#4111=VERTEX_POINT('',#28835);
#4112=VERTEX_POINT('',#28839);
#4113=VERTEX_POINT('',#28843);
#4114=VERTEX_POINT('',#28846);
#4115=VERTEX_POINT('',#28850);
#4116=VERTEX_POINT('',#28854);
#4117=VERTEX_POINT('',#28862);
#4118=VERTEX_POINT('',#28864);
#4119=VERTEX_POINT('',#28866);
#4120=VERTEX_POINT('',#28870);
#4121=VERTEX_POINT('',#28874);
#4122=VERTEX_POINT('',#28878);
#4123=VERTEX_POINT('',#28882);
#4124=VERTEX_POINT('',#28897);
#4125=VERTEX_POINT('',#28899);
#5272=EDGE_CURVE('',#4110,#4111,#183,.T.);
#5273=EDGE_CURVE('',#4112,#4110,#184,.T.);
#5274=EDGE_CURVE('',#4112,#4113,#2580,.T.);
#5275=EDGE_CURVE('',#4113,#4113,#3424,.T.);
#5276=EDGE_CURVE('',#4114,#4112,#185,.T.);
#5277=EDGE_CURVE('',#4115,#4114,#186,.T.);
#5278=EDGE_CURVE('',#4116,#4115,#187,.T.);
#5279=EDGE_CURVE('',#4111,#4116,#188,.T.);
#5280=EDGE_CURVE('',#4117,#4117,#3425,.T.);
#5281=EDGE_CURVE('',#4117,#4118,#2581,.T.);
#5282=EDGE_CURVE('',#4119,#4118,#189,.T.);
#5283=EDGE_CURVE('',#4120,#4119,#190,.T.);
#5284=EDGE_CURVE('',#4121,#4120,#191,.T.);
#5285=EDGE_CURVE('',#4122,#4121,#192,.T.);
#5286=EDGE_CURVE('',#4123,#4122,#193,.T.);
#5287=EDGE_CURVE('',#4118,#4123,#194,.T.);
#5288=EDGE_CURVE('',#4114,#4123,#2582,.T.);
#5289=EDGE_CURVE('',#4115,#4122,#2583,.T.);
#5290=EDGE_CURVE('',#4112,#4118,#2584,.T.);
#5291=EDGE_CURVE('',#4110,#4119,#2585,.T.);
#5292=EDGE_CURVE('',#4124,#4124,#3426,.F.);
#5293=EDGE_CURVE('',#4124,#4125,#2586,.T.);
#5294=EDGE_CURVE('',#4125,#4125,#3427,.F.);
#5295=EDGE_CURVE('',#4111,#4120,#2587,.T.);
#5296=EDGE_CURVE('',#4116,#4121,#2588,.T.);
#7517=ORIENTED_EDGE('',*,*,#5272,.F.);
#7518=ORIENTED_EDGE('',*,*,#5273,.F.);
#7519=ORIENTED_EDGE('',*,*,#5274,.T.);
#7520=ORIENTED_EDGE('',*,*,#5275,.F.);
#7521=ORIENTED_EDGE('',*,*,#5274,.F.);
#7522=ORIENTED_EDGE('',*,*,#5276,.F.);
#7523=ORIENTED_EDGE('',*,*,#5277,.F.);
#7524=ORIENTED_EDGE('',*,*,#5278,.F.);
#7525=ORIENTED_EDGE('',*,*,#5279,.F.);
#7526=ORIENTED_EDGE('',*,*,#5280,.F.);
#7527=ORIENTED_EDGE('',*,*,#5281,.T.);
#7528=ORIENTED_EDGE('',*,*,#5282,.F.);
#7529=ORIENTED_EDGE('',*,*,#5283,.F.);
#7530=ORIENTED_EDGE('',*,*,#5284,.F.);
#7531=ORIENTED_EDGE('',*,*,#5285,.F.);
#7532=ORIENTED_EDGE('',*,*,#5286,.F.);
#7533=ORIENTED_EDGE('',*,*,#5287,.F.);
#7534=ORIENTED_EDGE('',*,*,#5281,.F.);
#7535=ORIENTED_EDGE('',*,*,#5277,.T.);
#7536=ORIENTED_EDGE('',*,*,#5288,.T.);
#7537=ORIENTED_EDGE('',*,*,#5286,.T.);
#7538=ORIENTED_EDGE('',*,*,#5289,.F.);
#7539=ORIENTED_EDGE('',*,*,#5276,.T.);
#7540=ORIENTED_EDGE('',*,*,#5290,.T.);
#7541=ORIENTED_EDGE('',*,*,#5287,.T.);
#7542=ORIENTED_EDGE('',*,*,#5288,.F.);
#7543=ORIENTED_EDGE('',*,*,#5273,.T.);
#7544=ORIENTED_EDGE('',*,*,#5291,.T.);
#7545=ORIENTED_EDGE('',*,*,#5282,.T.);
#7546=ORIENTED_EDGE('',*,*,#5290,.F.);
#7547=ORIENTED_EDGE('',*,*,#5292,.F.);
#7548=ORIENTED_EDGE('',*,*,#5293,.T.);
#7549=ORIENTED_EDGE('',*,*,#5294,.T.);
#7550=ORIENTED_EDGE('',*,*,#5293,.F.);
#7551=ORIENTED_EDGE('',*,*,#5272,.T.);
#7552=ORIENTED_EDGE('',*,*,#5295,.T.);
#7553=ORIENTED_EDGE('',*,*,#5283,.T.);
#7554=ORIENTED_EDGE('',*,*,#5291,.F.);
#7555=ORIENTED_EDGE('',*,*,#5278,.T.);
#7556=ORIENTED_EDGE('',*,*,#5289,.T.);
#7557=ORIENTED_EDGE('',*,*,#5285,.T.);
#7558=ORIENTED_EDGE('',*,*,#5296,.F.);
#7559=ORIENTED_EDGE('',*,*,#5279,.T.);
#7560=ORIENTED_EDGE('',*,*,#5296,.T.);
#7561=ORIENTED_EDGE('',*,*,#5284,.T.);
#7562=ORIENTED_EDGE('',*,*,#5295,.F.);
#7563=ORIENTED_EDGE('',*,*,#5280,.T.);
#7564=ORIENTED_EDGE('',*,*,#5292,.T.);
#7565=ORIENTED_EDGE('',*,*,#5275,.T.);
#7566=ORIENTED_EDGE('',*,*,#5294,.F.);
#8240=CYLINDRICAL_SURFACE('',#9578,0.338975);
#8677=ADVANCED_FACE('',(#1440),#201,.T.);
#8678=ADVANCED_FACE('',(#1441),#202,.T.);
#8679=ADVANCED_FACE('',(#1442),#1004,.T.);
#8680=ADVANCED_FACE('',(#1443),#1005,.T.);
#8681=ADVANCED_FACE('',(#1444),#1006,.T.);
#8682=ADVANCED_FACE('',(#1445),#8240,.F.);
#8683=ADVANCED_FACE('',(#1446),#1007,.T.);
#8684=ADVANCED_FACE('',(#1447),#1008,.T.);
#8685=ADVANCED_FACE('',(#1448),#1009,.T.);
#8686=ADVANCED_FACE('',(#1449,#847),#1010,.T.);
#8687=ADVANCED_FACE('',(#1450,#848),#1011,.F.);
#8795=CLOSED_SHELL('',(#8677,#8678,#8679,#8680,#8681,#8682,#8683,#8684,
#8685,#8686,#8687));
#9570=AXIS2_PLACEMENT_3D('',#28832,#11283,#11284);
#9571=AXIS2_PLACEMENT_3D('',#28833,#11285,#11286);
#9572=AXIS2_PLACEMENT_3D('',#28845,#11288,#11289);
#9573=AXIS2_PLACEMENT_3D('',#28861,#11290,#11291);
#9574=AXIS2_PLACEMENT_3D('',#28863,#11292,#11293);
#9575=AXIS2_PLACEMENT_3D('',#28889,#11295,#11296);
#9576=AXIS2_PLACEMENT_3D('',#28892,#11299,#11300);
#9577=AXIS2_PLACEMENT_3D('',#28894,#11302,#11303);
#9578=AXIS2_PLACEMENT_3D('',#28896,#11305,#11306);
#9579=AXIS2_PLACEMENT_3D('',#28898,#11307,#11308);
#9580=AXIS2_PLACEMENT_3D('',#28901,#11310,#11311);
#9581=AXIS2_PLACEMENT_3D('',#28902,#11312,#11313);
#9582=AXIS2_PLACEMENT_3D('',#28904,#11315,#11316);
#9583=AXIS2_PLACEMENT_3D('',#28906,#11318,#11319);
#9584=AXIS2_PLACEMENT_3D('',#28907,#11320,#11321);
#9585=AXIS2_PLACEMENT_3D('',#28908,#11322,#11323);
#11283=DIRECTION('axis',(0.,0.,1.));
#11284=DIRECTION('refdir',(1.,0.,0.));
#11285=DIRECTION('center_axis',(0.,1.,0.));
#11286=DIRECTION('ref_axis',(1.,0.,0.));
#11287=DIRECTION('',(0.866025403784439,-0.5,1.06057523872491E-16));
#11288=DIRECTION('center_axis',(0.,-1.,0.));
#11289=DIRECTION('ref_axis',(1.,0.,0.));
#11290=DIRECTION('center_axis',(0.,-1.,0.));
#11291=DIRECTION('ref_axis',(1.,0.,0.));
#11292=DIRECTION('center_axis',(0.,1.,0.));
#11293=DIRECTION('ref_axis',(1.,0.,0.));
#11294=DIRECTION('',(-0.866025403784439,-0.5,-1.06057523872491E-16));
#11295=DIRECTION('center_axis',(1.4792020664489E-16,0.,-1.));
#11296=DIRECTION('ref_axis',(-1.,0.,-1.4792020664489E-16));
#11297=DIRECTION('',(0.,1.,0.));
#11298=DIRECTION('',(0.,1.,0.));
#11299=DIRECTION('center_axis',(-0.866025403784439,0.,-0.5));
#11300=DIRECTION('ref_axis',(-0.5,0.,0.866025403784439));
#11301=DIRECTION('',(0.,1.,0.));
#11302=DIRECTION('center_axis',(-0.866025403784439,0.,0.5));
#11303=DIRECTION('ref_axis',(0.5,0.,0.866025403784439));
#11304=DIRECTION('',(0.,1.,0.));
#11305=DIRECTION('center_axis',(0.,1.,0.));
#11306=DIRECTION('ref_axis',(1.,0.,0.));
#11307=DIRECTION('center_axis',(0.,1.,0.));
#11308=DIRECTION('ref_axis',(1.,0.,0.));
#11309=DIRECTION('',(0.,-1.,0.));
#11310=DIRECTION('center_axis',(0.,1.,0.));
#11311=DIRECTION('ref_axis',(1.,0.,0.));
#11312=DIRECTION('center_axis',(-2.95840413289779E-16,0.,1.));
#11313=DIRECTION('ref_axis',(1.,0.,2.95840413289779E-16));
#11314=DIRECTION('',(0.,1.,0.));
#11315=DIRECTION('center_axis',(0.866025403784439,0.,-0.5));
#11316=DIRECTION('ref_axis',(-0.5,0.,-0.866025403784439));
#11317=DIRECTION('',(0.,1.,0.));
#11318=DIRECTION('center_axis',(0.866025403784439,0.,0.5));
#11319=DIRECTION('ref_axis',(0.5,0.,-0.866025403784439));
#11320=DIRECTION('center_axis',(0.,1.,0.));
#11321=DIRECTION('ref_axis',(1.,0.,0.));
#11322=DIRECTION('center_axis',(0.,1.,0.));
#11323=DIRECTION('ref_axis',(1.,0.,0.));
#28832=CARTESIAN_POINT('',(0.,0.,0.));
#28833=CARTESIAN_POINT('Origin',(0.,0.067277284513851,0.));
#28834=CARTESIAN_POINT('',(-0.375277674973257,0.0768195421087395,0.65));
#28835=CARTESIAN_POINT('',(0.375277674973257,0.0768195421087395,0.65));
#28836=CARTESIAN_POINT('Ctrl Pts',(-0.375277674973257,0.0768195421087395,
0.65));
#28837=CARTESIAN_POINT('Ctrl Pts',(1.66533453693773E-13,-0.0315137912242439,
0.65));
#28838=CARTESIAN_POINT('Ctrl Pts',(0.375277674973257,0.0768195421087394,
0.65));
#28839=CARTESIAN_POINT('',(-0.750555349946514,0.0768195421087394,-9.19165206894919E-17));
#28840=CARTESIAN_POINT('Ctrl Pts',(-0.750555349946514,0.0768195421087394,
-9.19165206894919E-17));
#28841=CARTESIAN_POINT('Ctrl Pts',(-0.562916512459802,-0.0315137912242434,
0.325000000000144));
#28842=CARTESIAN_POINT('Ctrl Pts',(-0.375277674973257,0.0768195421087395,
0.65));
#28843=CARTESIAN_POINT('',(-0.6175,-2.77555756156289E-17,-7.5621939847349E-17));
#28844=CARTESIAN_POINT('',(-0.734027674973257,0.067277284513851,-8.98924642641573E-17));
#28845=CARTESIAN_POINT('Origin',(0.,0.,0.));
#28846=CARTESIAN_POINT('',(-0.375277674973257,0.0768195421087395,-0.65));
#28847=CARTESIAN_POINT('Ctrl Pts',(-0.375277674973257,0.0768195421087395,
-0.65));
#28848=CARTESIAN_POINT('Ctrl Pts',(-0.562916512459968,-0.0315137912242437,
-0.324999999999856));
#28849=CARTESIAN_POINT('Ctrl Pts',(-0.750555349946514,0.0768195421087395,
-9.19165206894919E-17));
#28850=CARTESIAN_POINT('',(0.375277674973257,0.0768195421087395,-0.65));
#28851=CARTESIAN_POINT('Ctrl Pts',(0.375277674973257,0.0768195421087395,
-0.65));
#28852=CARTESIAN_POINT('Ctrl Pts',(-1.66144875635155E-13,-0.0315137912242437,
-0.65));
#28853=CARTESIAN_POINT('Ctrl Pts',(-0.375277674973257,0.0768195421087395,
-0.65));
#28854=CARTESIAN_POINT('',(0.750555349946514,0.0768195421087394,0.));
#28855=CARTESIAN_POINT('Ctrl Pts',(0.750555349946514,0.0768195421087394,
0.));
#28856=CARTESIAN_POINT('Ctrl Pts',(0.562916512459802,-0.0315137912242436,
-0.325000000000144));
#28857=CARTESIAN_POINT('Ctrl Pts',(0.375277674973257,0.0768195421087395,
-0.65));
#28858=CARTESIAN_POINT('Ctrl Pts',(0.375277674973257,0.0768195421087394,
0.65));
#28859=CARTESIAN_POINT('Ctrl Pts',(0.562916512459968,-0.0315137912242439,
0.324999999999856));
#28860=CARTESIAN_POINT('Ctrl Pts',(0.750555349946514,0.0768195421087394,
0.));
#28861=CARTESIAN_POINT('Origin',(0.,0.612722715486149,0.));
#28862=CARTESIAN_POINT('',(-0.6175,0.68,-7.5621939847349E-17));
#28863=CARTESIAN_POINT('Origin',(0.,0.68,0.));
#28864=CARTESIAN_POINT('',(-0.750555349946514,0.603180457891261,-9.19165206894919E-17));
#28865=CARTESIAN_POINT('',(-0.734027674973257,0.612722715486149,-8.98924642641573E-17));
#28866=CARTESIAN_POINT('',(-0.375277674973257,0.603180457891261,0.65));
#28867=CARTESIAN_POINT('Ctrl Pts',(-0.375277674973257,0.603180457891261,
0.65));
#28868=CARTESIAN_POINT('Ctrl Pts',(-0.562916512459968,0.711513791224243,
0.324999999999856));
#28869=CARTESIAN_POINT('Ctrl Pts',(-0.750555349946514,0.603180457891261,
-9.19165206894919E-17));
#28870=CARTESIAN_POINT('',(0.375277674973257,0.603180457891261,0.65));
#28871=CARTESIAN_POINT('Ctrl Pts',(0.375277674973257,0.603180457891261,
0.65));
#28872=CARTESIAN_POINT('Ctrl Pts',(-1.66755498298699E-13,0.711513791224244,
0.65));
#28873=CARTESIAN_POINT('Ctrl Pts',(-0.375277674973257,0.603180457891261,
0.65));
#28874=CARTESIAN_POINT('',(0.750555349946514,0.603180457891261,0.));
#28875=CARTESIAN_POINT('Ctrl Pts',(0.750555349946514,0.603180457891261,
0.));
#28876=CARTESIAN_POINT('Ctrl Pts',(0.562916512459802,0.711513791224244,
0.325000000000144));
#28877=CARTESIAN_POINT('Ctrl Pts',(0.375277674973257,0.603180457891261,
0.65));
#28878=CARTESIAN_POINT('',(0.375277674973257,0.603180457891261,-0.65));
#28879=CARTESIAN_POINT('Ctrl Pts',(0.375277674973257,0.603180457891261,
-0.65));
#28880=CARTESIAN_POINT('Ctrl Pts',(0.562916512459969,0.711513791224244,
-0.324999999999856));
#28881=CARTESIAN_POINT('Ctrl Pts',(0.750555349946514,0.603180457891261,
0.));
#28882=CARTESIAN_POINT('',(-0.375277674973257,0.603180457891261,-0.65));
#28883=CARTESIAN_POINT('Ctrl Pts',(-0.375277674973257,0.603180457891261,
-0.65));
#28884=CARTESIAN_POINT('Ctrl Pts',(1.66422431391311E-13,0.711513791224244,
-0.65));
#28885=CARTESIAN_POINT('Ctrl Pts',(0.375277674973257,0.603180457891261,
-0.65));
#28886=CARTESIAN_POINT('Ctrl Pts',(-0.750555349946514,0.603180457891261,
-9.19165206894919E-17));
#28887=CARTESIAN_POINT('Ctrl Pts',(-0.562916512459802,0.711513791224244,
-0.325000000000144));
#28888=CARTESIAN_POINT('Ctrl Pts',(-0.375277674973257,0.603180457891261,
-0.65));
#28889=CARTESIAN_POINT('Origin',(0.375277674973257,0.,-0.65));
#28890=CARTESIAN_POINT('',(-0.375277674973257,0.,-0.65));
#28891=CARTESIAN_POINT('',(0.375277674973257,0.,-0.65));
#28892=CARTESIAN_POINT('Origin',(-0.375277674973257,0.,-0.65));
#28893=CARTESIAN_POINT('',(-0.750555349946514,0.,-9.19165206894919E-17));
#28894=CARTESIAN_POINT('Origin',(-0.750555349946514,0.,-9.19165206894919E-17));
#28895=CARTESIAN_POINT('',(-0.375277674973257,0.,0.65));
#28896=CARTESIAN_POINT('Origin',(0.,0.,0.));
#28897=CARTESIAN_POINT('',(-0.338975,0.68,4.15124648740974E-17));
#28898=CARTESIAN_POINT('Origin',(0.,0.68,0.));
#28899=CARTESIAN_POINT('',(-0.338975,0.,4.15124648740974E-17));
#28900=CARTESIAN_POINT('',(-0.338975,0.,4.15124648740974E-17));
#28901=CARTESIAN_POINT('Origin',(0.,0.,0.));
#28902=CARTESIAN_POINT('Origin',(-0.375277674973257,0.,0.65));
#28903=CARTESIAN_POINT('',(0.375277674973257,0.,0.65));
#28904=CARTESIAN_POINT('Origin',(0.750555349946514,0.,0.));
#28905=CARTESIAN_POINT('',(0.750555349946514,0.,0.));
#28906=CARTESIAN_POINT('Origin',(0.375277674973257,0.,0.65));
#28907=CARTESIAN_POINT('Origin',(0.,0.68,-1.11022302462516E-16));
#28908=CARTESIAN_POINT('Origin',(0.,0.,-1.11022302462516E-16));
#34395=UNCERTAINTY_MEASURE_WITH_UNIT(LENGTH_MEASURE(0.001),#34434,
'DISTANCE_ACCURACY_VALUE',
'Maximum model space distance between geometric entities at asserted c
onnectivities');
#34404=UNCERTAINTY_MEASURE_WITH_UNIT(LENGTH_MEASURE(0.001),#34434,
'DISTANCE_ACCURACY_VALUE',
'Maximum model space distance between geometric entities at asserted c
onnectivities');
#34424=(
GEOMETRIC_REPRESENTATION_CONTEXT(3)
GLOBAL_UNCERTAINTY_ASSIGNED_CONTEXT((#34395))
GLOBAL_UNIT_ASSIGNED_CONTEXT((#34434,#34436,#34437))
REPRESENTATION_CONTEXT('','3D')
);
#34433=(
GEOMETRIC_REPRESENTATION_CONTEXT(3)
GLOBAL_UNCERTAINTY_ASSIGNED_CONTEXT((#34404))
GLOBAL_UNIT_ASSIGNED_CONTEXT((#34434,#34436,#34437))
REPRESENTATION_CONTEXT('','3D')
);
#34434=(
LENGTH_UNIT()
NAMED_UNIT(*)
SI_UNIT(.CENTI.,.METRE.)
);
#34436=(
NAMED_UNIT(*)
PLANE_ANGLE_UNIT()
SI_UNIT($,.RADIAN.)
);
#34437=(
NAMED_UNIT(*)
SI_UNIT($,.STERADIAN.)
SOLID_ANGLE_UNIT()
);
#34457=SHAPE_DEFINITION_REPRESENTATION(#34485,#34556);
#34485=PRODUCT_DEFINITION_SHAPE('',$,#34585);
#34556=SHAPE_REPRESENTATION('',(#9570),#34424);
#34565=PRODUCT_DEFINITION_CONTEXT('part definition',#34651,'design');
#34585=PRODUCT_DEFINITION('Hex Nut - M8','Hex Nut - M8',#34613,#34565);
#34613=PRODUCT_DEFINITION_FORMATION('',$,#34672);
#34651=APPLICATION_CONTEXT(
'Core Data for Automotive Mechanical Design Process');
#34652=PRODUCT_CONTEXT('part definition',#34651,'mechanical');
#34672=PRODUCT('Hex Nut - M8','Hex Nut - M8','Hex Nut - M8',(#34652));
#34744=COLOUR_RGB('Black',0.12,0.14,0.17);
#34745=FILL_AREA_STYLE_COLOUR('',#34744);
#34746=FILL_AREA_STYLE('',(#34745));
#34747=SURFACE_STYLE_FILL_AREA(#34746);
#34748=SURFACE_SIDE_STYLE('',(#34747));
#34749=SURFACE_STYLE_USAGE(.BOTH.,#34748);
#34750=PRESENTATION_STYLE_ASSIGNMENT((#34749));
ENDSEC;
END-ISO-10303-21;
